ISO-10303-21;
HEADER;
/* Generated by software containing ST-Developer
 * from STEP Tools, Inc. (www.steptools.com) 
 */

FILE_DESCRIPTION(
/* description */ (''),
/* implementation_level */ '2;1');

FILE_NAME(
/* name */ 'PO7.step',
/* time_stamp */ '2026-10-06T10:18:54-07:00',
/* author */ (''),
/* organization */ (''),
/* preprocessor_version */ 'ST-DEVELOPER v20.2',
/* originating_system */ 'Autodesk Translation Framework v15.15.0.0',
/* authorisation */ '');

FILE_SCHEMA (('AUTOMOTIVE_DESIGN { 1 0 10303 214 3 1 1 }'));
ENDSEC;

DATA;
#10=MECHANICAL_DESIGN_GEOMETRIC_PRESENTATION_REPRESENTATION('',(#85),#8445);
#67=SHAPE_REPRESENTATION_RELATIONSHIP('SRR','None',#8488,#76);
#76=ADVANCED_BREP_SHAPE_REPRESENTATION('',(#94),#8440);
#85=STYLED_ITEM('',(#8537),#94);
#94=MANIFOLD_SOLID_BREP('Body1',#4006);
#153=CYLINDRICAL_SURFACE('',#4409,9.5);
#154=CYLINDRICAL_SURFACE('',#4411,6.5);
#360=FACE_BOUND('',#975,.T.);
#476=CIRCLE('',#4392,6.5);
#477=CIRCLE('',#4393,9.5);
#478=CIRCLE('',#4399,6.5);
#479=CIRCLE('',#4400,9.5);
#480=CIRCLE('',#4402,6.5);
#481=CIRCLE('',#4403,6.5);
#482=CIRCLE('',#4404,9.5);
#483=CIRCLE('',#4405,9.5);
#484=CIRCLE('',#4407,9.5);
#485=CIRCLE('',#4408,6.5);
#486=CIRCLE('',#4410,9.5);
#487=CIRCLE('',#4412,6.5);
#706=FACE_OUTER_BOUND('',#964,.T.);
#707=FACE_OUTER_BOUND('',#965,.T.);
#708=FACE_OUTER_BOUND('',#966,.T.);
#709=FACE_OUTER_BOUND('',#967,.T.);
#710=FACE_OUTER_BOUND('',#968,.T.);
#711=FACE_OUTER_BOUND('',#969,.T.);
#712=FACE_OUTER_BOUND('',#970,.T.);
#713=FACE_OUTER_BOUND('',#971,.T.);
#714=FACE_OUTER_BOUND('',#972,.T.);
#715=FACE_OUTER_BOUND('',#973,.T.);
#716=FACE_OUTER_BOUND('',#974,.T.);
#964=EDGE_LOOP('',(#3413,#3414,#3415,#3416));
#965=EDGE_LOOP('',(#3417,#3418,#3419,#3420));
#966=EDGE_LOOP('',(#3421,#3422,#3423,#3424));
#967=EDGE_LOOP('',(#3425,#3426,#3427,#3428));
#968=EDGE_LOOP('',(#3429,#3430,#3431,#3432));
#969=EDGE_LOOP('',(#3433,#3434,#3435,#3436));
#970=EDGE_LOOP('',(#3437,#3438,#3439,#3440,#3441,#3442));
#971=EDGE_LOOP('',(#3443,#3444,#3445,#3446));
#972=EDGE_LOOP('',(#3447,#3448,#3449,#3450,#3451,#3452,#3453,#3454,#3455,
#3456,#3457,#3458));
#973=EDGE_LOOP('',(#3459,#3460,#3461,#3462,#3463,#3464,#3465,#3466,#3467,
#3468,#3469,#3470));
#974=EDGE_LOOP('',(#3471));
#975=EDGE_LOOP('',(#3472));
#1247=LINE('',#8157,#1536);
#1248=LINE('',#8160,#1537);
#1249=LINE('',#8163,#1538);
#1250=LINE('',#8165,#1539);
#1251=LINE('',#8166,#1540);
#1252=LINE('',#8170,#1541);
#1253=LINE('',#8172,#1542);
#1254=LINE('',#8174,#1543);
#1255=LINE('',#8175,#1544);
#1256=LINE('',#8178,#1545);
#1257=LINE('',#8180,#1546);
#1258=LINE('',#8181,#1547);
#1259=LINE('',#8185,#1548);
#1260=LINE('',#8187,#1549);
#1261=LINE('',#8189,#1550);
#1262=LINE('',#8190,#1551);
#1263=LINE('',#8206,#1552);
#1264=LINE('',#8210,#1553);
#1536=VECTOR('',#5296,10.);
#1537=VECTOR('',#5299,10.);
#1538=VECTOR('',#5302,10.);
#1539=VECTOR('',#5303,10.);
#1540=VECTOR('',#5304,10.);
#1541=VECTOR('',#5307,10.);
#1542=VECTOR('',#5308,10.);
#1543=VECTOR('',#5309,10.);
#1544=VECTOR('',#5310,10.);
#1545=VECTOR('',#5313,10.);
#1546=VECTOR('',#5314,10.);
#1547=VECTOR('',#5315,10.);
#1548=VECTOR('',#5318,10.);
#1549=VECTOR('',#5319,10.);
#1550=VECTOR('',#5320,10.);
#1551=VECTOR('',#5321,10.);
#1552=VECTOR('',#5346,9.5);
#1553=VECTOR('',#5351,6.5);
#1884=VERTEX_POINT('',#8153);
#1885=VERTEX_POINT('',#8154);
#1886=VERTEX_POINT('',#8156);
#1887=VERTEX_POINT('',#8158);
#1888=VERTEX_POINT('',#8162);
#1889=VERTEX_POINT('',#8164);
#1890=VERTEX_POINT('',#8168);
#1891=VERTEX_POINT('',#8169);
#1892=VERTEX_POINT('',#8171);
#1893=VERTEX_POINT('',#8173);
#1894=VERTEX_POINT('',#8177);
#1895=VERTEX_POINT('',#8179);
#1896=VERTEX_POINT('',#8183);
#1897=VERTEX_POINT('',#8184);
#1898=VERTEX_POINT('',#8186);
#1899=VERTEX_POINT('',#8188);
#1900=VERTEX_POINT('',#8195);
#1901=VERTEX_POINT('',#8198);
#1902=VERTEX_POINT('',#8205);
#1903=VERTEX_POINT('',#8209);
#2407=EDGE_CURVE('',#1884,#1885,#476,.T.);
#2408=EDGE_CURVE('',#1884,#1886,#1247,.T.);
#2409=EDGE_CURVE('',#1887,#1886,#477,.T.);
#2410=EDGE_CURVE('',#1885,#1887,#1248,.T.);
#2411=EDGE_CURVE('',#1888,#1884,#1249,.T.);
#2412=EDGE_CURVE('',#1889,#1888,#1250,.T.);
#2413=EDGE_CURVE('',#1886,#1889,#1251,.T.);
#2414=EDGE_CURVE('',#1890,#1891,#1252,.T.);
#2415=EDGE_CURVE('',#1892,#1890,#1253,.T.);
#2416=EDGE_CURVE('',#1893,#1892,#1254,.T.);
#2417=EDGE_CURVE('',#1891,#1893,#1255,.T.);
#2418=EDGE_CURVE('',#1885,#1894,#1256,.T.);
#2419=EDGE_CURVE('',#1895,#1887,#1257,.T.);
#2420=EDGE_CURVE('',#1894,#1895,#1258,.T.);
#2421=EDGE_CURVE('',#1896,#1897,#1259,.T.);
#2422=EDGE_CURVE('',#1898,#1896,#1260,.T.);
#2423=EDGE_CURVE('',#1899,#1898,#1261,.T.);
#2424=EDGE_CURVE('',#1899,#1897,#1262,.T.);
#2425=EDGE_CURVE('',#1897,#1890,#478,.T.);
#2426=EDGE_CURVE('',#1892,#1899,#479,.T.);
#2427=EDGE_CURVE('',#1896,#1900,#480,.T.);
#2428=EDGE_CURVE('',#1900,#1894,#481,.T.);
#2429=EDGE_CURVE('',#1895,#1901,#482,.T.);
#2430=EDGE_CURVE('',#1901,#1898,#483,.T.);
#2431=EDGE_CURVE('',#1893,#1889,#484,.T.);
#2432=EDGE_CURVE('',#1888,#1891,#485,.T.);
#2433=EDGE_CURVE('',#1901,#1902,#1263,.T.);
#2434=EDGE_CURVE('',#1902,#1902,#486,.T.);
#2435=EDGE_CURVE('',#1900,#1903,#1264,.T.);
#2436=EDGE_CURVE('',#1903,#1903,#487,.T.);
#3413=ORIENTED_EDGE('',*,*,#2407,.F.);
#3414=ORIENTED_EDGE('',*,*,#2408,.T.);
#3415=ORIENTED_EDGE('',*,*,#2409,.F.);
#3416=ORIENTED_EDGE('',*,*,#2410,.F.);
#3417=ORIENTED_EDGE('',*,*,#2411,.F.);
#3418=ORIENTED_EDGE('',*,*,#2412,.F.);
#3419=ORIENTED_EDGE('',*,*,#2413,.F.);
#3420=ORIENTED_EDGE('',*,*,#2408,.F.);
#3421=ORIENTED_EDGE('',*,*,#2414,.F.);
#3422=ORIENTED_EDGE('',*,*,#2415,.F.);
#3423=ORIENTED_EDGE('',*,*,#2416,.F.);
#3424=ORIENTED_EDGE('',*,*,#2417,.F.);
#3425=ORIENTED_EDGE('',*,*,#2418,.F.);
#3426=ORIENTED_EDGE('',*,*,#2410,.T.);
#3427=ORIENTED_EDGE('',*,*,#2419,.F.);
#3428=ORIENTED_EDGE('',*,*,#2420,.F.);
#3429=ORIENTED_EDGE('',*,*,#2421,.F.);
#3430=ORIENTED_EDGE('',*,*,#2422,.F.);
#3431=ORIENTED_EDGE('',*,*,#2423,.F.);
#3432=ORIENTED_EDGE('',*,*,#2424,.T.);
#3433=ORIENTED_EDGE('',*,*,#2425,.F.);
#3434=ORIENTED_EDGE('',*,*,#2424,.F.);
#3435=ORIENTED_EDGE('',*,*,#2426,.F.);
#3436=ORIENTED_EDGE('',*,*,#2415,.T.);
#3437=ORIENTED_EDGE('',*,*,#2422,.T.);
#3438=ORIENTED_EDGE('',*,*,#2427,.T.);
#3439=ORIENTED_EDGE('',*,*,#2428,.T.);
#3440=ORIENTED_EDGE('',*,*,#2420,.T.);
#3441=ORIENTED_EDGE('',*,*,#2429,.T.);
#3442=ORIENTED_EDGE('',*,*,#2430,.T.);
#3443=ORIENTED_EDGE('',*,*,#2417,.T.);
#3444=ORIENTED_EDGE('',*,*,#2431,.T.);
#3445=ORIENTED_EDGE('',*,*,#2412,.T.);
#3446=ORIENTED_EDGE('',*,*,#2432,.T.);
#3447=ORIENTED_EDGE('',*,*,#2416,.T.);
#3448=ORIENTED_EDGE('',*,*,#2426,.T.);
#3449=ORIENTED_EDGE('',*,*,#2423,.T.);
#3450=ORIENTED_EDGE('',*,*,#2430,.F.);
#3451=ORIENTED_EDGE('',*,*,#2433,.T.);
#3452=ORIENTED_EDGE('',*,*,#2434,.T.);
#3453=ORIENTED_EDGE('',*,*,#2433,.F.);
#3454=ORIENTED_EDGE('',*,*,#2429,.F.);
#3455=ORIENTED_EDGE('',*,*,#2419,.T.);
#3456=ORIENTED_EDGE('',*,*,#2409,.T.);
#3457=ORIENTED_EDGE('',*,*,#2413,.T.);
#3458=ORIENTED_EDGE('',*,*,#2431,.F.);
#3459=ORIENTED_EDGE('',*,*,#2414,.T.);
#3460=ORIENTED_EDGE('',*,*,#2432,.F.);
#3461=ORIENTED_EDGE('',*,*,#2411,.T.);
#3462=ORIENTED_EDGE('',*,*,#2407,.T.);
#3463=ORIENTED_EDGE('',*,*,#2418,.T.);
#3464=ORIENTED_EDGE('',*,*,#2428,.F.);
#3465=ORIENTED_EDGE('',*,*,#2435,.T.);
#3466=ORIENTED_EDGE('',*,*,#2436,.F.);
#3467=ORIENTED_EDGE('',*,*,#2435,.F.);
#3468=ORIENTED_EDGE('',*,*,#2427,.F.);
#3469=ORIENTED_EDGE('',*,*,#2421,.T.);
#3470=ORIENTED_EDGE('',*,*,#2425,.T.);
#3471=ORIENTED_EDGE('',*,*,#2434,.F.);
#3472=ORIENTED_EDGE('',*,*,#2436,.T.);
#3730=PLANE('',#4391);
#3731=PLANE('',#4394);
#3732=PLANE('',#4395);
#3733=PLANE('',#4396);
#3734=PLANE('',#4397);
#3735=PLANE('',#4398);
#3736=PLANE('',#4401);
#3737=PLANE('',#4406);
#3738=PLANE('',#4413);
#3947=ADVANCED_FACE('',(#706),#3730,.F.);
#3948=ADVANCED_FACE('',(#707),#3731,.F.);
#3949=ADVANCED_FACE('',(#708),#3732,.F.);
#3950=ADVANCED_FACE('',(#709),#3733,.F.);
#3951=ADVANCED_FACE('',(#710),#3734,.F.);
#3952=ADVANCED_FACE('',(#711),#3735,.F.);
#3953=ADVANCED_FACE('',(#712),#3736,.T.);
#3954=ADVANCED_FACE('',(#713),#3737,.T.);
#3955=ADVANCED_FACE('',(#714),#153,.T.);
#3956=ADVANCED_FACE('',(#715),#154,.F.);
#3957=ADVANCED_FACE('',(#716,#360),#3738,.F.);
#4006=CLOSED_SHELL('',(#3947,#3948,#3949,#3950,#3951,#3952,#3953,#3954,
#3955,#3956,#3957));
#4390=AXIS2_PLACEMENT_3D('',#8151,#5290,#5291);
#4391=AXIS2_PLACEMENT_3D('',#8152,#5292,#5293);
#4392=AXIS2_PLACEMENT_3D('',#8155,#5294,#5295);
#4393=AXIS2_PLACEMENT_3D('',#8159,#5297,#5298);
#4394=AXIS2_PLACEMENT_3D('',#8161,#5300,#5301);
#4395=AXIS2_PLACEMENT_3D('',#8167,#5305,#5306);
#4396=AXIS2_PLACEMENT_3D('',#8176,#5311,#5312);
#4397=AXIS2_PLACEMENT_3D('',#8182,#5316,#5317);
#4398=AXIS2_PLACEMENT_3D('',#8191,#5322,#5323);
#4399=AXIS2_PLACEMENT_3D('',#8192,#5324,#5325);
#4400=AXIS2_PLACEMENT_3D('',#8193,#5326,#5327);
#4401=AXIS2_PLACEMENT_3D('',#8194,#5328,#5329);
#4402=AXIS2_PLACEMENT_3D('',#8196,#5330,#5331);
#4403=AXIS2_PLACEMENT_3D('',#8197,#5332,#5333);
#4404=AXIS2_PLACEMENT_3D('',#8199,#5334,#5335);
#4405=AXIS2_PLACEMENT_3D('',#8200,#5336,#5337);
#4406=AXIS2_PLACEMENT_3D('',#8201,#5338,#5339);
#4407=AXIS2_PLACEMENT_3D('',#8202,#5340,#5341);
#4408=AXIS2_PLACEMENT_3D('',#8203,#5342,#5343);
#4409=AXIS2_PLACEMENT_3D('',#8204,#5344,#5345);
#4410=AXIS2_PLACEMENT_3D('',#8207,#5347,#5348);
#4411=AXIS2_PLACEMENT_3D('',#8208,#5349,#5350);
#4412=AXIS2_PLACEMENT_3D('',#8211,#5352,#5353);
#4413=AXIS2_PLACEMENT_3D('',#8212,#5354,#5355);
#5290=DIRECTION('axis',(0.,0.,1.));
#5291=DIRECTION('refdir',(1.,0.,0.));
#5292=DIRECTION('center_axis',(-1.,0.,0.));
#5293=DIRECTION('ref_axis',(0.,-1.,0.));
#5294=DIRECTION('center_axis',(1.,0.,0.));
#5295=DIRECTION('ref_axis',(0.,1.,0.));
#5296=DIRECTION('',(0.,0.,1.));
#5297=DIRECTION('center_axis',(-1.,0.,0.));
#5298=DIRECTION('ref_axis',(0.,1.,0.));
#5299=DIRECTION('',(0.,0.,1.));
#5300=DIRECTION('center_axis',(0.,1.,0.));
#5301=DIRECTION('ref_axis',(-1.,0.,0.));
#5302=DIRECTION('',(-1.,0.,0.));
#5303=DIRECTION('',(0.,0.,-1.));
#5304=DIRECTION('',(1.,0.,0.));
#5305=DIRECTION('center_axis',(0.,1.,0.));
#5306=DIRECTION('ref_axis',(-1.,0.,0.));
#5307=DIRECTION('',(1.,0.,0.));
#5308=DIRECTION('',(0.,0.,1.));
#5309=DIRECTION('',(-1.,0.,0.));
#5310=DIRECTION('',(0.,0.,-1.));
#5311=DIRECTION('center_axis',(-4.20539024479226E-17,-1.,0.));
#5312=DIRECTION('ref_axis',(1.,-4.20539024479226E-17,0.));
#5313=DIRECTION('',(1.,0.,0.));
#5314=DIRECTION('',(-1.,0.,0.));
#5315=DIRECTION('',(0.,0.,1.));
#5316=DIRECTION('center_axis',(-4.20539024479226E-17,-1.,0.));
#5317=DIRECTION('ref_axis',(1.,-4.20539024479226E-17,0.));
#5318=DIRECTION('',(-1.,0.,0.));
#5319=DIRECTION('',(0.,0.,1.));
#5320=DIRECTION('',(1.,0.,0.));
#5321=DIRECTION('',(0.,0.,1.));
#5322=DIRECTION('center_axis',(-1.,0.,0.));
#5323=DIRECTION('ref_axis',(0.,-1.,0.));
#5324=DIRECTION('center_axis',(1.,0.,0.));
#5325=DIRECTION('ref_axis',(0.,1.,0.));
#5326=DIRECTION('center_axis',(-1.,0.,0.));
#5327=DIRECTION('ref_axis',(0.,1.,0.));
#5328=DIRECTION('center_axis',(1.,0.,0.));
#5329=DIRECTION('ref_axis',(0.,1.,0.));
#5330=DIRECTION('center_axis',(-1.,0.,0.));
#5331=DIRECTION('ref_axis',(0.,1.,0.));
#5332=DIRECTION('center_axis',(-1.,0.,0.));
#5333=DIRECTION('ref_axis',(0.,1.,0.));
#5334=DIRECTION('center_axis',(1.,0.,0.));
#5335=DIRECTION('ref_axis',(0.,1.,0.));
#5336=DIRECTION('center_axis',(1.,0.,0.));
#5337=DIRECTION('ref_axis',(0.,1.,0.));
#5338=DIRECTION('center_axis',(1.,0.,0.));
#5339=DIRECTION('ref_axis',(0.,1.,0.));
#5340=DIRECTION('center_axis',(1.,0.,0.));
#5341=DIRECTION('ref_axis',(0.,1.,0.));
#5342=DIRECTION('center_axis',(-1.,0.,0.));
#5343=DIRECTION('ref_axis',(0.,1.,0.));
#5344=DIRECTION('center_axis',(1.,0.,0.));
#5345=DIRECTION('ref_axis',(0.,1.,0.));
#5346=DIRECTION('',(-1.,0.,0.));
#5347=DIRECTION('center_axis',(1.,0.,0.));
#5348=DIRECTION('ref_axis',(0.,1.,0.));
#5349=DIRECTION('center_axis',(-1.,0.,0.));
#5350=DIRECTION('ref_axis',(0.,1.,0.));
#5351=DIRECTION('',(-1.,0.,0.));
#5352=DIRECTION('center_axis',(1.,0.,0.));
#5353=DIRECTION('ref_axis',(0.,1.,0.));
#5354=DIRECTION('center_axis',(1.,0.,0.));
#5355=DIRECTION('ref_axis',(0.,1.,0.));
#8151=CARTESIAN_POINT('',(0.,0.,0.));
#8152=CARTESIAN_POINT('Origin',(16.7000002980232,1.49222526803142,0.));
#8153=CARTESIAN_POINT('',(16.7000002980232,1.49222526803142,6.3263942138827));
#8154=CARTESIAN_POINT('',(16.7000002980232,-0.90777473196858,6.43629901698168));
#8155=CARTESIAN_POINT('Origin',(16.7000002980232,0.,0.));
#8156=CARTESIAN_POINT('',(16.7000002980232,1.49222526803142,9.38207139972024));
#8157=CARTESIAN_POINT('',(16.7000002980232,1.49222526803142,0.));
#8158=CARTESIAN_POINT('',(16.7000002980232,-0.90777473196858,9.45652922778751));
#8159=CARTESIAN_POINT('Origin',(16.7000002980232,0.,0.));
#8160=CARTESIAN_POINT('',(16.7000002980232,-0.90777473196858,0.));
#8161=CARTESIAN_POINT('Origin',(20.0000002980232,1.49222526803142,0.));
#8162=CARTESIAN_POINT('',(20.0000002980232,1.49222526803142,6.3263942138827));
#8163=CARTESIAN_POINT('',(9.,1.49222526803142,6.3263942138827));
#8164=CARTESIAN_POINT('',(20.0000002980232,1.49222526803142,9.38207139972024));
#8165=CARTESIAN_POINT('',(20.,1.49222526803142,0.));
#8166=CARTESIAN_POINT('',(0.,1.49222526803142,9.38207139972024));
#8167=CARTESIAN_POINT('Origin',(20.0000002980232,1.49222526803142,0.));
#8168=CARTESIAN_POINT('',(16.7000002980232,1.49222526803142,-6.3263942138827));
#8169=CARTESIAN_POINT('',(20.0000002980232,1.49222526803142,-6.3263942138827));
#8170=CARTESIAN_POINT('',(9.,1.49222526803142,-6.3263942138827));
#8171=CARTESIAN_POINT('',(16.7000002980232,1.49222526803142,-9.38207139972024));
#8172=CARTESIAN_POINT('',(16.7000002980232,1.49222526803142,0.));
#8173=CARTESIAN_POINT('',(20.0000002980232,1.49222526803142,-9.38207139972024));
#8174=CARTESIAN_POINT('',(0.,1.49222526803142,-9.38207139972024));
#8175=CARTESIAN_POINT('',(20.,1.49222526803142,0.));
#8176=CARTESIAN_POINT('Origin',(16.7000002980232,-0.90777473196858,0.));
#8177=CARTESIAN_POINT('',(20.0000002980232,-0.90777473196858,6.43629901698168));
#8178=CARTESIAN_POINT('',(9.,-0.90777473196858,6.43629901698168));
#8179=CARTESIAN_POINT('',(20.0000002980232,-0.90777473196858,9.45652922778751));
#8180=CARTESIAN_POINT('',(0.,-0.90777473196858,9.45652922778751));
#8181=CARTESIAN_POINT('',(20.,-0.90777473196858,0.));
#8182=CARTESIAN_POINT('Origin',(16.7000002980232,-0.90777473196858,0.));
#8183=CARTESIAN_POINT('',(20.0000002980232,-0.90777473196858,-6.43629901698168));
#8184=CARTESIAN_POINT('',(16.7000002980232,-0.90777473196858,-6.43629901698168));
#8185=CARTESIAN_POINT('',(9.,-0.90777473196858,-6.43629901698168));
#8186=CARTESIAN_POINT('',(20.0000002980232,-0.90777473196858,-9.45652922778751));
#8187=CARTESIAN_POINT('',(20.,-0.90777473196858,0.));
#8188=CARTESIAN_POINT('',(16.7000002980232,-0.90777473196858,-9.45652922778751));
#8189=CARTESIAN_POINT('',(0.,-0.90777473196858,-9.45652922778751));
#8190=CARTESIAN_POINT('',(16.7000002980232,-0.90777473196858,0.));
#8191=CARTESIAN_POINT('Origin',(16.7000002980232,1.49222526803142,0.));
#8192=CARTESIAN_POINT('Origin',(16.7000002980232,0.,0.));
#8193=CARTESIAN_POINT('Origin',(16.7000002980232,0.,0.));
#8194=CARTESIAN_POINT('Origin',(20.,0.,0.));
#8195=CARTESIAN_POINT('',(20.0000002980232,-6.5,7.9602041944578E-16));
#8196=CARTESIAN_POINT('Origin',(20.,0.,0.));
#8197=CARTESIAN_POINT('Origin',(20.,0.,0.));
#8198=CARTESIAN_POINT('',(20.0000002980232,-9.5,-1.16341445918999E-15));
#8199=CARTESIAN_POINT('Origin',(20.,0.,0.));
#8200=CARTESIAN_POINT('Origin',(20.,0.,0.));
#8201=CARTESIAN_POINT('Origin',(20.,0.,0.));
#8202=CARTESIAN_POINT('Origin',(20.,0.,0.));
#8203=CARTESIAN_POINT('Origin',(20.,0.,0.));
#8204=CARTESIAN_POINT('Origin',(0.,0.,0.));
#8205=CARTESIAN_POINT('',(0.,-9.5,-1.16341445918999E-15));
#8206=CARTESIAN_POINT('',(0.,-9.5,-1.16341445918999E-15));
#8207=CARTESIAN_POINT('Origin',(0.,0.,0.));
#8208=CARTESIAN_POINT('Origin',(9.,0.,0.));
#8209=CARTESIAN_POINT('',(0.,-6.5,-7.9602041944578E-16));
#8210=CARTESIAN_POINT('',(9.,-6.5,7.9602041944578E-16));
#8211=CARTESIAN_POINT('Origin',(0.,0.,0.));
#8212=CARTESIAN_POINT('Origin',(0.,0.,0.));
#8429=UNCERTAINTY_MEASURE_WITH_UNIT(LENGTH_MEASURE(0.01),#8446,
'DISTANCE_ACCURACY_VALUE',
'Maximum model space distance between geometric entities at asserted c
onnectivities');
#8434=UNCERTAINTY_MEASURE_WITH_UNIT(LENGTH_MEASURE(0.01),#8446,
'DISTANCE_ACCURACY_VALUE',
'Maximum model space distance between geometric entities at asserted c
onnectivities');
#8440=(
GEOMETRIC_REPRESENTATION_CONTEXT(3)
GLOBAL_UNCERTAINTY_ASSIGNED_CONTEXT((#8429))
GLOBAL_UNIT_ASSIGNED_CONTEXT((#8446,#8448,#8449))
REPRESENTATION_CONTEXT('','3D')
);
#8445=(
GEOMETRIC_REPRESENTATION_CONTEXT(3)
GLOBAL_UNCERTAINTY_ASSIGNED_CONTEXT((#8434))
GLOBAL_UNIT_ASSIGNED_CONTEXT((#8446,#8448,#8449))
REPRESENTATION_CONTEXT('','3D')
);
#8446=(
LENGTH_UNIT()
NAMED_UNIT(*)
SI_UNIT(.MILLI.,.METRE.)
);
#8448=(
NAMED_UNIT(*)
PLANE_ANGLE_UNIT()
SI_UNIT($,.RADIAN.)
);
#8449=(
NAMED_UNIT(*)
SI_UNIT($,.STERADIAN.)
SOLID_ANGLE_UNIT()
);
#8455=SHAPE_DEFINITION_REPRESENTATION(#8465,#8488);
#8465=PRODUCT_DEFINITION_SHAPE('',$,#8499);
#8488=SHAPE_REPRESENTATION('',(#4390),#8440);
#8493=PRODUCT_DEFINITION_CONTEXT('part definition',#8525,'design');
#8499=PRODUCT_DEFINITION('2026-10-05-11-51-15-560','PO7',#8509,#8493);
#8509=PRODUCT_DEFINITION_FORMATION('',$,#8532);
#8525=APPLICATION_CONTEXT(
'Core Data for Automotive Mechanical Design Process');
#8526=PRODUCT_CONTEXT('part definition',#8525,'mechanical');
#8532=PRODUCT('2026-10-05-11-51-15-560','PO7',$,(#8526));
#8537=PRESENTATION_STYLE_ASSIGNMENT((#8538));
#8538=SURFACE_STYLE_USAGE(.BOTH.,#8539);
#8539=SURFACE_SIDE_STYLE('',(#8540));
#8540=SURFACE_STYLE_FILL_AREA(#8541);
#8541=FILL_AREA_STYLE('Steel - Satin',(#8542));
#8542=FILL_AREA_STYLE_COLOUR('Steel - Satin',#8543);
#8543=COLOUR_RGB('Steel - Satin', 0.09019608, 0.27058824, 0.51372549);
ENDSEC;
END-ISO-10303-21;
